ISO-10303-21;
HEADER;
/* Generated by software containing ST-Developer
 * from STEP Tools, Inc. (www.steptools.com) 
 */

FILE_DESCRIPTION(
/* description */ ('Worm-less right-angle friction wheel drive'),
/* implementation_level */ '2;1');

FILE_NAME(
/* name */ 'Bearing cap (3).step',
/* time_stamp */ '2026-10-28T03:22:36-07:00',
/* author */ (''),
/* organization */ (''),
/* preprocessor_version */ 'ST-DEVELOPER v20.2',
/* originating_system */ 'Autodesk Translation Framework v15.17.0.0',
/* authorisation */ '');

FILE_SCHEMA (('AUTOMOTIVE_DESIGN { 1 0 10303 214 3 1 1 }'));
ENDSEC;

DATA;
#10=MECHANICAL_DESIGN_GEOMETRIC_PRESENTATION_REPRESENTATION('',(#620),#17046);
#526=SHAPE_REPRESENTATION_RELATIONSHIP('SRR','None',#17269,#573);
#573=ADVANCED_BREP_SHAPE_REPRESENTATION('',(#674),#17005);
#620=STYLED_ITEM('',(#17591),#674);
#674=MANIFOLD_SOLID_BREP('Body1',#8175);
#812=FACE_BOUND('',#1895,.T.);
#813=FACE_BOUND('',#1899,.T.);
#814=FACE_BOUND('',#1900,.T.);
#815=FACE_BOUND('',#1901,.T.);
#816=FACE_BOUND('',#1902,.T.);
#817=FACE_BOUND('',#1903,.T.);
#818=FACE_BOUND('',#1905,.T.);
#819=FACE_BOUND('',#1906,.T.);
#820=FACE_BOUND('',#1907,.T.);
#821=FACE_BOUND('',#1908,.T.);
#822=FACE_BOUND('',#1909,.T.);
#1013=PLANE('',#9001);
#1014=PLANE('',#9008);
#1015=PLANE('',#9009);
#1326=FACE_OUTER_BOUND('',#1889,.T.);
#1327=FACE_OUTER_BOUND('',#1890,.T.);
#1328=FACE_OUTER_BOUND('',#1891,.T.);
#1329=FACE_OUTER_BOUND('',#1892,.T.);
#1330=FACE_OUTER_BOUND('',#1893,.T.);
#1331=FACE_OUTER_BOUND('',#1894,.T.);
#1332=FACE_OUTER_BOUND('',#1896,.T.);
#1333=FACE_OUTER_BOUND('',#1897,.T.);
#1334=FACE_OUTER_BOUND('',#1898,.T.);
#1335=FACE_OUTER_BOUND('',#1904,.T.);
#1889=EDGE_LOOP('',(#6116,#6117,#6118,#6119));
#1890=EDGE_LOOP('',(#6120,#6121,#6122,#6123));
#1891=EDGE_LOOP('',(#6124,#6125,#6126,#6127));
#1892=EDGE_LOOP('',(#6128,#6129,#6130,#6131));
#1893=EDGE_LOOP('',(#6132,#6133,#6134,#6135));
#1894=EDGE_LOOP('',(#6136));
#1895=EDGE_LOOP('',(#6137));
#1896=EDGE_LOOP('',(#6138,#6139,#6140,#6141));
#1897=EDGE_LOOP('',(#6142,#6143,#6144,#6145));
#1898=EDGE_LOOP('',(#6146));
#1899=EDGE_LOOP('',(#6147));
#1900=EDGE_LOOP('',(#6148));
#1901=EDGE_LOOP('',(#6149));
#1902=EDGE_LOOP('',(#6150));
#1903=EDGE_LOOP('',(#6151));
#1904=EDGE_LOOP('',(#6152));
#1905=EDGE_LOOP('',(#6153));
#1906=EDGE_LOOP('',(#6154));
#1907=EDGE_LOOP('',(#6155));
#1908=EDGE_LOOP('',(#6156));
#1909=EDGE_LOOP('',(#6157));
#2554=LINE('',#12994,#3094);
#2555=LINE('',#13000,#3095);
#2556=LINE('',#13006,#3096);
#2557=LINE('',#13012,#3097);
#2558=LINE('',#13018,#3098);
#2559=LINE('',#13026,#3099);
#2560=LINE('',#13031,#3100);
#3094=VECTOR('',#10442,0.225);
#3095=VECTOR('',#10449,0.225);
#3096=VECTOR('',#10456,0.225);
#3097=VECTOR('',#10463,0.225);
#3098=VECTOR('',#10470,1.59);
#3099=VECTOR('',#10481,1.2);
#3100=VECTOR('',#10486,2.4);
#3571=CIRCLE('',#8987,0.225);
#3572=CIRCLE('',#8988,0.225);
#3573=CIRCLE('',#8990,0.225);
#3574=CIRCLE('',#8991,0.225);
#3575=CIRCLE('',#8993,0.225);
#3576=CIRCLE('',#8994,0.225);
#3577=CIRCLE('',#8996,0.225);
#3578=CIRCLE('',#8997,0.225);
#3579=CIRCLE('',#8999,1.59);
#3580=CIRCLE('',#9000,1.59);
#3581=CIRCLE('',#9002,1.2);
#3582=CIRCLE('',#9004,1.2);
#3583=CIRCLE('',#9006,2.4);
#3584=CIRCLE('',#9007,2.4);
#4063=VERTEX_POINT('',#12991);
#4064=VERTEX_POINT('',#12993);
#4065=VERTEX_POINT('',#12997);
#4066=VERTEX_POINT('',#12999);
#4067=VERTEX_POINT('',#13003);
#4068=VERTEX_POINT('',#13005);
#4069=VERTEX_POINT('',#13009);
#4070=VERTEX_POINT('',#13011);
#4071=VERTEX_POINT('',#13015);
#4072=VERTEX_POINT('',#13017);
#4073=VERTEX_POINT('',#13021);
#4074=VERTEX_POINT('',#13024);
#4075=VERTEX_POINT('',#13028);
#4076=VERTEX_POINT('',#13030);
#4827=EDGE_CURVE('',#4063,#4063,#3571,.T.);
#4828=EDGE_CURVE('',#4063,#4064,#2554,.T.);
#4829=EDGE_CURVE('',#4064,#4064,#3572,.T.);
#4830=EDGE_CURVE('',#4065,#4065,#3573,.T.);
#4831=EDGE_CURVE('',#4065,#4066,#2555,.T.);
#4832=EDGE_CURVE('',#4066,#4066,#3574,.T.);
#4833=EDGE_CURVE('',#4067,#4067,#3575,.T.);
#4834=EDGE_CURVE('',#4067,#4068,#2556,.T.);
#4835=EDGE_CURVE('',#4068,#4068,#3576,.T.);
#4836=EDGE_CURVE('',#4069,#4069,#3577,.T.);
#4837=EDGE_CURVE('',#4069,#4070,#2557,.T.);
#4838=EDGE_CURVE('',#4070,#4070,#3578,.T.);
#4839=EDGE_CURVE('',#4071,#4071,#3579,.T.);
#4840=EDGE_CURVE('',#4071,#4072,#2558,.T.);
#4841=EDGE_CURVE('',#4072,#4072,#3580,.T.);
#4842=EDGE_CURVE('',#4073,#4073,#3581,.T.);
#4843=EDGE_CURVE('',#4074,#4074,#3582,.T.);
#4844=EDGE_CURVE('',#4074,#4073,#2559,.T.);
#4845=EDGE_CURVE('',#4075,#4075,#3583,.T.);
#4846=EDGE_CURVE('',#4075,#4076,#2560,.T.);
#4847=EDGE_CURVE('',#4076,#4076,#3584,.T.);
#6116=ORIENTED_EDGE('',*,*,#4827,.F.);
#6117=ORIENTED_EDGE('',*,*,#4828,.T.);
#6118=ORIENTED_EDGE('',*,*,#4829,.F.);
#6119=ORIENTED_EDGE('',*,*,#4828,.F.);
#6120=ORIENTED_EDGE('',*,*,#4830,.F.);
#6121=ORIENTED_EDGE('',*,*,#4831,.T.);
#6122=ORIENTED_EDGE('',*,*,#4832,.F.);
#6123=ORIENTED_EDGE('',*,*,#4831,.F.);
#6124=ORIENTED_EDGE('',*,*,#4833,.F.);
#6125=ORIENTED_EDGE('',*,*,#4834,.T.);
#6126=ORIENTED_EDGE('',*,*,#4835,.F.);
#6127=ORIENTED_EDGE('',*,*,#4834,.F.);
#6128=ORIENTED_EDGE('',*,*,#4836,.F.);
#6129=ORIENTED_EDGE('',*,*,#4837,.T.);
#6130=ORIENTED_EDGE('',*,*,#4838,.F.);
#6131=ORIENTED_EDGE('',*,*,#4837,.F.);
#6132=ORIENTED_EDGE('',*,*,#4839,.F.);
#6133=ORIENTED_EDGE('',*,*,#4840,.T.);
#6134=ORIENTED_EDGE('',*,*,#4841,.T.);
#6135=ORIENTED_EDGE('',*,*,#4840,.F.);
#6136=ORIENTED_EDGE('',*,*,#4841,.F.);
#6137=ORIENTED_EDGE('',*,*,#4842,.F.);
#6138=ORIENTED_EDGE('',*,*,#4843,.F.);
#6139=ORIENTED_EDGE('',*,*,#4844,.T.);
#6140=ORIENTED_EDGE('',*,*,#4842,.T.);
#6141=ORIENTED_EDGE('',*,*,#4844,.F.);
#6142=ORIENTED_EDGE('',*,*,#4845,.F.);
#6143=ORIENTED_EDGE('',*,*,#4846,.T.);
#6144=ORIENTED_EDGE('',*,*,#4847,.T.);
#6145=ORIENTED_EDGE('',*,*,#4846,.F.);
#6146=ORIENTED_EDGE('',*,*,#4845,.T.);
#6147=ORIENTED_EDGE('',*,*,#4843,.T.);
#6148=ORIENTED_EDGE('',*,*,#4838,.T.);
#6149=ORIENTED_EDGE('',*,*,#4835,.T.);
#6150=ORIENTED_EDGE('',*,*,#4832,.T.);
#6151=ORIENTED_EDGE('',*,*,#4829,.T.);
#6152=ORIENTED_EDGE('',*,*,#4847,.F.);
#6153=ORIENTED_EDGE('',*,*,#4839,.T.);
#6154=ORIENTED_EDGE('',*,*,#4836,.T.);
#6155=ORIENTED_EDGE('',*,*,#4833,.T.);
#6156=ORIENTED_EDGE('',*,*,#4830,.T.);
#6157=ORIENTED_EDGE('',*,*,#4827,.T.);
#7587=CYLINDRICAL_SURFACE('',#8986,0.225);
#7588=CYLINDRICAL_SURFACE('',#8989,0.225);
#7589=CYLINDRICAL_SURFACE('',#8992,0.225);
#7590=CYLINDRICAL_SURFACE('',#8995,0.225);
#7591=CYLINDRICAL_SURFACE('',#8998,1.59);
#7592=CYLINDRICAL_SURFACE('',#9003,1.2);
#7593=CYLINDRICAL_SURFACE('',#9005,2.4);
#7818=ADVANCED_FACE('',(#1326),#7587,.F.);
#7819=ADVANCED_FACE('',(#1327),#7588,.F.);
#7820=ADVANCED_FACE('',(#1328),#7589,.F.);
#7821=ADVANCED_FACE('',(#1329),#7590,.F.);
#7822=ADVANCED_FACE('',(#1330),#7591,.T.);
#7823=ADVANCED_FACE('',(#1331,#812),#1013,.F.);
#7824=ADVANCED_FACE('',(#1332),#7592,.F.);
#7825=ADVANCED_FACE('',(#1333),#7593,.T.);
#7826=ADVANCED_FACE('',(#1334,#813,#814,#815,#816,#817),#1014,.T.);
#7827=ADVANCED_FACE('',(#1335,#818,#819,#820,#821,#822),#1015,.F.);
#8175=CLOSED_SHELL('',(#7818,#7819,#7820,#7821,#7822,#7823,#7824,#7825,
#7826,#7827));
#8985=AXIS2_PLACEMENT_3D('',#12989,#10436,#10437);
#8986=AXIS2_PLACEMENT_3D('',#12990,#10438,#10439);
#8987=AXIS2_PLACEMENT_3D('',#12992,#10440,#10441);
#8988=AXIS2_PLACEMENT_3D('',#12995,#10443,#10444);
#8989=AXIS2_PLACEMENT_3D('',#12996,#10445,#10446);
#8990=AXIS2_PLACEMENT_3D('',#12998,#10447,#10448);
#8991=AXIS2_PLACEMENT_3D('',#13001,#10450,#10451);
#8992=AXIS2_PLACEMENT_3D('',#13002,#10452,#10453);
#8993=AXIS2_PLACEMENT_3D('',#13004,#10454,#10455);
#8994=AXIS2_PLACEMENT_3D('',#13007,#10457,#10458);
#8995=AXIS2_PLACEMENT_3D('',#13008,#10459,#10460);
#8996=AXIS2_PLACEMENT_3D('',#13010,#10461,#10462);
#8997=AXIS2_PLACEMENT_3D('',#13013,#10464,#10465);
#8998=AXIS2_PLACEMENT_3D('',#13014,#10466,#10467);
#8999=AXIS2_PLACEMENT_3D('',#13016,#10468,#10469);
#9000=AXIS2_PLACEMENT_3D('',#13019,#10471,#10472);
#9001=AXIS2_PLACEMENT_3D('',#13020,#10473,#10474);
#9002=AXIS2_PLACEMENT_3D('',#13022,#10475,#10476);
#9003=AXIS2_PLACEMENT_3D('',#13023,#10477,#10478);
#9004=AXIS2_PLACEMENT_3D('',#13025,#10479,#10480);
#9005=AXIS2_PLACEMENT_3D('',#13027,#10482,#10483);
#9006=AXIS2_PLACEMENT_3D('',#13029,#10484,#10485);
#9007=AXIS2_PLACEMENT_3D('',#13032,#10487,#10488);
#9008=AXIS2_PLACEMENT_3D('',#13033,#10489,#10490);
#9009=AXIS2_PLACEMENT_3D('',#13034,#10491,#10492);
#10436=DIRECTION('axis',(0.,0.,1.));
#10437=DIRECTION('refdir',(1.,0.,0.));
#10438=DIRECTION('center_axis',(0.,1.,0.));
#10439=DIRECTION('ref_axis',(1.,0.,0.));
#10440=DIRECTION('center_axis',(0.,1.,0.));
#10441=DIRECTION('ref_axis',(1.,0.,0.));
#10442=DIRECTION('',(0.,1.,0.));
#10443=DIRECTION('center_axis',(0.,-1.,0.));
#10444=DIRECTION('ref_axis',(1.,0.,0.));
#10445=DIRECTION('center_axis',(0.,1.,0.));
#10446=DIRECTION('ref_axis',(1.,0.,0.));
#10447=DIRECTION('center_axis',(0.,1.,0.));
#10448=DIRECTION('ref_axis',(1.,0.,0.));
#10449=DIRECTION('',(0.,1.,0.));
#10450=DIRECTION('center_axis',(0.,-1.,0.));
#10451=DIRECTION('ref_axis',(1.,0.,0.));
#10452=DIRECTION('center_axis',(0.,1.,0.));
#10453=DIRECTION('ref_axis',(1.,0.,0.));
#10454=DIRECTION('center_axis',(0.,1.,0.));
#10455=DIRECTION('ref_axis',(1.,0.,0.));
#10456=DIRECTION('',(0.,1.,0.));
#10457=DIRECTION('center_axis',(0.,-1.,0.));
#10458=DIRECTION('ref_axis',(1.,0.,0.));
#10459=DIRECTION('center_axis',(0.,1.,0.));
#10460=DIRECTION('ref_axis',(1.,0.,0.));
#10461=DIRECTION('center_axis',(0.,1.,0.));
#10462=DIRECTION('ref_axis',(1.,0.,0.));
#10463=DIRECTION('',(0.,1.,0.));
#10464=DIRECTION('center_axis',(0.,-1.,0.));
#10465=DIRECTION('ref_axis',(1.,0.,0.));
#10466=DIRECTION('center_axis',(0.,1.,0.));
#10467=DIRECTION('ref_axis',(1.,0.,0.));
#10468=DIRECTION('center_axis',(0.,1.,0.));
#10469=DIRECTION('ref_axis',(1.,0.,0.));
#10470=DIRECTION('',(0.,-1.,0.));
#10471=DIRECTION('center_axis',(0.,1.,0.));
#10472=DIRECTION('ref_axis',(1.,0.,0.));
#10473=DIRECTION('center_axis',(0.,1.,0.));
#10474=DIRECTION('ref_axis',(1.,0.,0.));
#10475=DIRECTION('center_axis',(0.,-1.,0.));
#10476=DIRECTION('ref_axis',(1.,0.,0.));
#10477=DIRECTION('center_axis',(0.,1.,0.));
#10478=DIRECTION('ref_axis',(1.,0.,0.));
#10479=DIRECTION('center_axis',(0.,-1.,0.));
#10480=DIRECTION('ref_axis',(1.,0.,0.));
#10481=DIRECTION('',(0.,-1.,0.));
#10482=DIRECTION('center_axis',(0.,1.,0.));
#10483=DIRECTION('ref_axis',(1.,0.,0.));
#10484=DIRECTION('center_axis',(0.,1.,0.));
#10485=DIRECTION('ref_axis',(1.,0.,0.));
#10486=DIRECTION('',(0.,-1.,0.));
#10487=DIRECTION('center_axis',(0.,1.,0.));
#10488=DIRECTION('ref_axis',(1.,0.,0.));
#10489=DIRECTION('center_axis',(0.,1.,0.));
#10490=DIRECTION('ref_axis',(1.,0.,0.));
#10491=DIRECTION('center_axis',(0.,1.,0.));
#10492=DIRECTION('ref_axis',(1.,0.,0.));
#12989=CARTESIAN_POINT('',(0.,0.,0.));
#12990=CARTESIAN_POINT('Origin',(-1.48492424049175,-3.3,5.51507575950825));
#12991=CARTESIAN_POINT('',(-1.70992424049175,-3.2,5.51507575950825));
#12992=CARTESIAN_POINT('Origin',(-1.48492424049175,-3.2,5.51507575950825));
#12993=CARTESIAN_POINT('',(-1.70992424049175,-3.,5.51507575950825));
#12994=CARTESIAN_POINT('',(-1.70992424049175,-3.3,5.51507575950825));
#12995=CARTESIAN_POINT('Origin',(-1.48492424049175,-3.,5.51507575950825));
#12996=CARTESIAN_POINT('Origin',(-1.48492424049175,-3.3,8.48492424049175));
#12997=CARTESIAN_POINT('',(-1.70992424049175,-3.2,8.48492424049175));
#12998=CARTESIAN_POINT('Origin',(-1.48492424049175,-3.2,8.48492424049175));
#12999=CARTESIAN_POINT('',(-1.70992424049175,-3.,8.48492424049175));
#13000=CARTESIAN_POINT('',(-1.70992424049175,-3.3,8.48492424049175));
#13001=CARTESIAN_POINT('Origin',(-1.48492424049175,-3.,8.48492424049175));
#13002=CARTESIAN_POINT('Origin',(1.48492424049175,-3.3,8.48492424049175));
#13003=CARTESIAN_POINT('',(1.25992424049175,-3.2,8.48492424049175));
#13004=CARTESIAN_POINT('Origin',(1.48492424049175,-3.2,8.48492424049175));
#13005=CARTESIAN_POINT('',(1.25992424049175,-3.,8.48492424049175));
#13006=CARTESIAN_POINT('',(1.25992424049175,-3.3,8.48492424049175));
#13007=CARTESIAN_POINT('Origin',(1.48492424049175,-3.,8.48492424049175));
#13008=CARTESIAN_POINT('Origin',(1.48492424049175,-3.3,5.51507575950825));
#13009=CARTESIAN_POINT('',(1.25992424049175,-3.2,5.51507575950825));
#13010=CARTESIAN_POINT('Origin',(1.48492424049175,-3.2,5.51507575950825));
#13011=CARTESIAN_POINT('',(1.25992424049175,-3.,5.51507575950825));
#13012=CARTESIAN_POINT('',(1.25992424049175,-3.3,5.51507575950825));
#13013=CARTESIAN_POINT('Origin',(1.48492424049175,-3.,5.51507575950825));
#13014=CARTESIAN_POINT('Origin',(0.,-3.5,7.));
#13015=CARTESIAN_POINT('',(-1.59,-3.2,7.));
#13016=CARTESIAN_POINT('Origin',(0.,-3.2,7.));
#13017=CARTESIAN_POINT('',(-1.59,-3.5,7.));
#13018=CARTESIAN_POINT('',(-1.59,-3.5,7.));
#13019=CARTESIAN_POINT('Origin',(0.,-3.5,7.));
#13020=CARTESIAN_POINT('Origin',(0.,-3.5,7.));
#13021=CARTESIAN_POINT('',(-1.2,-3.5,7.));
#13022=CARTESIAN_POINT('Origin',(0.,-3.5,7.));
#13023=CARTESIAN_POINT('Origin',(0.,-3.2,7.));
#13024=CARTESIAN_POINT('',(-1.2,-3.,7.));
#13025=CARTESIAN_POINT('Origin',(0.,-3.,7.));
#13026=CARTESIAN_POINT('',(-1.2,-3.2,7.));
#13027=CARTESIAN_POINT('Origin',(0.,-3.2,7.));
#13028=CARTESIAN_POINT('',(-2.4,-3.,7.));
#13029=CARTESIAN_POINT('Origin',(0.,-3.,7.));
#13030=CARTESIAN_POINT('',(-2.4,-3.2,7.));
#13031=CARTESIAN_POINT('',(-2.4,-3.2,7.));
#13032=CARTESIAN_POINT('Origin',(0.,-3.2,7.));
#13033=CARTESIAN_POINT('Origin',(0.,-3.,7.));
#13034=CARTESIAN_POINT('Origin',(0.,-3.2,7.));
#16952=UNCERTAINTY_MEASURE_WITH_UNIT(LENGTH_MEASURE(0.001),#17047,
'DISTANCE_ACCURACY_VALUE',
'Maximum model space distance between geometric entities at asserted c
onnectivities');
#16993=UNCERTAINTY_MEASURE_WITH_UNIT(LENGTH_MEASURE(0.001),#17047,
'DISTANCE_ACCURACY_VALUE',
'Maximum model space distance between geometric entities at asserted c
onnectivities');
#17005=(
GEOMETRIC_REPRESENTATION_CONTEXT(3)
GLOBAL_UNCERTAINTY_ASSIGNED_CONTEXT((#16952))
GLOBAL_UNIT_ASSIGNED_CONTEXT((#17047,#17049,#17050))
REPRESENTATION_CONTEXT('','3D')
);
#17046=(
GEOMETRIC_REPRESENTATION_CONTEXT(3)
GLOBAL_UNCERTAINTY_ASSIGNED_CONTEXT((#16993))
GLOBAL_UNIT_ASSIGNED_CONTEXT((#17047,#17049,#17050))
REPRESENTATION_CONTEXT('','3D')
);
#17047=(
LENGTH_UNIT()
NAMED_UNIT(*)
SI_UNIT(.CENTI.,.METRE.)
);
#17049=(
NAMED_UNIT(*)
PLANE_ANGLE_UNIT()
SI_UNIT($,.RADIAN.)
);
#17050=(
NAMED_UNIT(*)
SI_UNIT($,.STERADIAN.)
SOLID_ANGLE_UNIT()
);
#17062=SHAPE_DEFINITION_REPRESENTATION(#17114,#17269);
#17114=PRODUCT_DEFINITION_SHAPE('',$,#17322);
#17269=SHAPE_REPRESENTATION('',(#8985),#17005);
#17310=PRODUCT_DEFINITION_CONTEXT('part definition',#17468,'design');
#17322=PRODUCT_DEFINITION('Bearing cap (3)','Bearing cap (3)',#17374,#17310);
#17374=PRODUCT_DEFINITION_FORMATION('',$,#17481);
#17468=APPLICATION_CONTEXT(
'Core Data for Automotive Mechanical Design Process');
#17469=PRODUCT_CONTEXT('part definition',#17468,'mechanical');
#17481=PRODUCT('Bearing cap (3)','Bearing cap (3)','Bearing cap (3)',(#17469));
#17585=COLOUR_RGB('Grey',0.48,0.52,0.57);
#17586=FILL_AREA_STYLE_COLOUR('',#17585);
#17587=FILL_AREA_STYLE('',(#17586));
#17588=SURFACE_STYLE_FILL_AREA(#17587);
#17589=SURFACE_SIDE_STYLE('',(#17588));
#17590=SURFACE_STYLE_USAGE(.BOTH.,#17589);
#17591=PRESENTATION_STYLE_ASSIGNMENT((#17590));
ENDSEC;
END-ISO-10303-21;
